ISO-10303-21;
HEADER;
/* Generated by software containing ST-Developer
 * from STEP Tools, Inc. (www.steptools.com) 
 */

FILE_DESCRIPTION(
/* description */ ('PAT-083'),
/* implementation_level */ '2;1');

FILE_NAME(
/* name */ 'Lower diaphragm plate.step',
/* time_stamp */ '2026-10-29T20:18:00-07:00',
/* author */ (''),
/* organization */ (''),
/* preprocessor_version */ 'ST-DEVELOPER v20.2',
/* originating_system */ 'Autodesk Translation Framework v15.17.0.0',
/* authorisation */ '');

FILE_SCHEMA (('AUTOMOTIVE_DESIGN { 1 0 10303 214 3 1 1 }'));
ENDSEC;

DATA;
#10=MECHANICAL_DESIGN_GEOMETRIC_PRESENTATION_REPRESENTATION('',(#237),#8428);
#189=SHAPE_REPRESENTATION_RELATIONSHIP('SRR','None',#8523,#213);
#213=ADVANCED_BREP_SHAPE_REPRESENTATION('',(#261),#8412);
#237=STYLED_ITEM('',(#8719),#261);
#261=MANIFOLD_SOLID_BREP('Body1',#3683);
#304=FACE_BOUND('',#839,.T.);
#305=FACE_BOUND('',#841,.T.);
#403=PLANE('',#4120);
#404=PLANE('',#4121);
#574=FACE_OUTER_BOUND('',#836,.T.);
#575=FACE_OUTER_BOUND('',#837,.T.);
#576=FACE_OUTER_BOUND('',#838,.T.);
#577=FACE_OUTER_BOUND('',#840,.T.);
#836=EDGE_LOOP('',(#2744,#2745,#2746,#2747));
#837=EDGE_LOOP('',(#2748,#2749,#2750,#2751));
#838=EDGE_LOOP('',(#2752));
#839=EDGE_LOOP('',(#2753));
#840=EDGE_LOOP('',(#2754));
#841=EDGE_LOOP('',(#2755));
#1115=LINE('',#6815,#1359);
#1116=LINE('',#6821,#1360);
#1359=VECTOR('',#4809,0.16);
#1360=VECTOR('',#4816,2.2);
#1590=CIRCLE('',#4115,0.16);
#1591=CIRCLE('',#4116,0.16);
#1592=CIRCLE('',#4118,2.2);
#1593=CIRCLE('',#4119,2.2);
#1803=VERTEX_POINT('',#6812);
#1804=VERTEX_POINT('',#6814);
#1805=VERTEX_POINT('',#6818);
#1806=VERTEX_POINT('',#6820);
#2148=EDGE_CURVE('',#1803,#1803,#1590,.T.);
#2149=EDGE_CURVE('',#1803,#1804,#1115,.T.);
#2150=EDGE_CURVE('',#1804,#1804,#1591,.T.);
#2151=EDGE_CURVE('',#1805,#1805,#1592,.T.);
#2152=EDGE_CURVE('',#1805,#1806,#1116,.T.);
#2153=EDGE_CURVE('',#1806,#1806,#1593,.T.);
#2744=ORIENTED_EDGE('',*,*,#2148,.F.);
#2745=ORIENTED_EDGE('',*,*,#2149,.T.);
#2746=ORIENTED_EDGE('',*,*,#2150,.T.);
#2747=ORIENTED_EDGE('',*,*,#2149,.F.);
#2748=ORIENTED_EDGE('',*,*,#2151,.F.);
#2749=ORIENTED_EDGE('',*,*,#2152,.T.);
#2750=ORIENTED_EDGE('',*,*,#2153,.T.);
#2751=ORIENTED_EDGE('',*,*,#2152,.F.);
#2752=ORIENTED_EDGE('',*,*,#2151,.T.);
#2753=ORIENTED_EDGE('',*,*,#2148,.T.);
#2754=ORIENTED_EDGE('',*,*,#2153,.F.);
#2755=ORIENTED_EDGE('',*,*,#2150,.F.);
#3395=CYLINDRICAL_SURFACE('',#4114,0.16);
#3396=CYLINDRICAL_SURFACE('',#4117,2.2);
#3521=ADVANCED_FACE('',(#574),#3395,.F.);
#3522=ADVANCED_FACE('',(#575),#3396,.T.);
#3523=ADVANCED_FACE('',(#576,#304),#403,.T.);
#3524=ADVANCED_FACE('',(#577,#305),#404,.F.);
#3683=CLOSED_SHELL('',(#3521,#3522,#3523,#3524));
#4113=AXIS2_PLACEMENT_3D('',#6810,#4803,#4804);
#4114=AXIS2_PLACEMENT_3D('',#6811,#4805,#4806);
#4115=AXIS2_PLACEMENT_3D('',#6813,#4807,#4808);
#4116=AXIS2_PLACEMENT_3D('',#6816,#4810,#4811);
#4117=AXIS2_PLACEMENT_3D('',#6817,#4812,#4813);
#4118=AXIS2_PLACEMENT_3D('',#6819,#4814,#4815);
#4119=AXIS2_PLACEMENT_3D('',#6822,#4817,#4818);
#4120=AXIS2_PLACEMENT_3D('',#6823,#4819,#4820);
#4121=AXIS2_PLACEMENT_3D('',#6824,#4821,#4822);
#4803=DIRECTION('axis',(0.,0.,1.));
#4804=DIRECTION('refdir',(1.,0.,0.));
#4805=DIRECTION('center_axis',(0.,0.,1.));
#4806=DIRECTION('ref_axis',(1.,0.,0.));
#4807=DIRECTION('center_axis',(0.,0.,-1.));
#4808=DIRECTION('ref_axis',(1.,0.,0.));
#4809=DIRECTION('',(0.,0.,-1.));
#4810=DIRECTION('center_axis',(0.,0.,-1.));
#4811=DIRECTION('ref_axis',(1.,0.,0.));
#4812=DIRECTION('center_axis',(0.,0.,1.));
#4813=DIRECTION('ref_axis',(1.,0.,0.));
#4814=DIRECTION('center_axis',(0.,0.,1.));
#4815=DIRECTION('ref_axis',(1.,0.,0.));
#4816=DIRECTION('',(0.,0.,-1.));
#4817=DIRECTION('center_axis',(0.,0.,1.));
#4818=DIRECTION('ref_axis',(1.,0.,0.));
#4819=DIRECTION('center_axis',(0.,0.,1.));
#4820=DIRECTION('ref_axis',(1.,0.,0.));
#4821=DIRECTION('center_axis',(0.,0.,1.));
#4822=DIRECTION('ref_axis',(1.,0.,0.));
#6810=CARTESIAN_POINT('',(0.,0.,0.));
#6811=CARTESIAN_POINT('Origin',(0.,0.,4.8));
#6812=CARTESIAN_POINT('',(-0.16,-1.95943487863577E-17,5.));
#6813=CARTESIAN_POINT('Origin',(0.,0.,5.));
#6814=CARTESIAN_POINT('',(-0.16,-1.95943487863577E-17,4.8));
#6815=CARTESIAN_POINT('',(-0.16,-1.95943487863577E-17,4.8));
#6816=CARTESIAN_POINT('Origin',(0.,0.,4.8));
#6817=CARTESIAN_POINT('Origin',(0.,0.,4.8));
#6818=CARTESIAN_POINT('',(-2.2,-2.69422295812418E-16,5.));
#6819=CARTESIAN_POINT('Origin',(0.,0.,5.));
#6820=CARTESIAN_POINT('',(-2.2,-2.69422295812418E-16,4.8));
#6821=CARTESIAN_POINT('',(-2.2,-2.69422295812418E-16,4.8));
#6822=CARTESIAN_POINT('Origin',(0.,0.,4.8));
#6823=CARTESIAN_POINT('Origin',(0.,0.,5.));
#6824=CARTESIAN_POINT('Origin',(0.,0.,4.8));
#8386=UNCERTAINTY_MEASURE_WITH_UNIT(LENGTH_MEASURE(0.001),#8429,
'DISTANCE_ACCURACY_VALUE',
'Maximum model space distance between geometric entities at asserted c
onnectivities');
#8402=UNCERTAINTY_MEASURE_WITH_UNIT(LENGTH_MEASURE(0.001),#8429,
'DISTANCE_ACCURACY_VALUE',
'Maximum model space distance between geometric entities at asserted c
onnectivities');
#8412=(
GEOMETRIC_REPRESENTATION_CONTEXT(3)
GLOBAL_UNCERTAINTY_ASSIGNED_CONTEXT((#8386))
GLOBAL_UNIT_ASSIGNED_CONTEXT((#8429,#8431,#8432))
REPRESENTATION_CONTEXT('','3D')
);
#8428=(
GEOMETRIC_REPRESENTATION_CONTEXT(3)
GLOBAL_UNCERTAINTY_ASSIGNED_CONTEXT((#8402))
GLOBAL_UNIT_ASSIGNED_CONTEXT((#8429,#8431,#8432))
REPRESENTATION_CONTEXT('','3D')
);
#8429=(
LENGTH_UNIT()
NAMED_UNIT(*)
SI_UNIT(.CENTI.,.METRE.)
);
#8431=(
NAMED_UNIT(*)
PLANE_ANGLE_UNIT()
SI_UNIT($,.RADIAN.)
);
#8432=(
NAMED_UNIT(*)
SI_UNIT($,.STERADIAN.)
SOLID_ANGLE_UNIT()
);
#8442=SHAPE_DEFINITION_REPRESENTATION(#8467,#8523);
#8467=PRODUCT_DEFINITION_SHAPE('',$,#8549);
#8523=SHAPE_REPRESENTATION('',(#4113),#8412);
#8539=PRODUCT_DEFINITION_CONTEXT('part definition',#8616,'design');
#8549=PRODUCT_DEFINITION('Lower diaphragm plate',
'Lower diaphragm plate',#8574,#8539);
#8574=PRODUCT_DEFINITION_FORMATION('',$,#8627);
#8616=APPLICATION_CONTEXT(
'Core Data for Automotive Mechanical Design Process');
#8617=PRODUCT_CONTEXT('part definition',#8616,'mechanical');
#8627=PRODUCT('Lower diaphragm plate','Lower diaphragm plate',
'Lower diaphragm plate',(#8617));
#8713=COLOUR_RGB('Off White',0.89,0.88,0.83);
#8714=FILL_AREA_STYLE_COLOUR('',#8713);
#8715=FILL_AREA_STYLE('',(#8714));
#8716=SURFACE_STYLE_FILL_AREA(#8715);
#8717=SURFACE_SIDE_STYLE('',(#8716));
#8718=SURFACE_STYLE_USAGE(.BOTH.,#8717);
#8719=PRESENTATION_STYLE_ASSIGNMENT((#8718));
ENDSEC;
END-ISO-10303-21;
